ISO-10303-21;
HEADER;
/* Generated by software containing ST-Developer
 * from STEP Tools, Inc. (www.steptools.com) 
 */

FILE_DESCRIPTION(
/* description */ (''),
/* implementation_level */ '2;1');

FILE_NAME(
/* name */ 'Clamp_04.step',
/* time_stamp */ '2026-10-22T13:39:42+06:00',
/* author */ (''),
/* organization */ (''),
/* preprocessor_version */ 'ST-DEVELOPER v20.2',
/* originating_system */ 'Autodesk Translation Framework v15.15.0.0',
/* authorisation */ '');

FILE_SCHEMA (('AUTOMOTIVE_DESIGN { 1 0 10303 214 3 1 1 }'));
ENDSEC;

DATA;
#10=MECHANICAL_DESIGN_GEOMETRIC_PRESENTATION_REPRESENTATION('',(#316),#17836);
#203=SPHERICAL_SURFACE('',#10946,0.299999999999994);
#204=SPHERICAL_SURFACE('',#10957,0.3);
#205=SPHERICAL_SURFACE('',#10961,0.299999999999994);
#206=SPHERICAL_SURFACE('',#10966,0.3);
#207=SPHERICAL_SURFACE('',#10970,0.300000000000011);
#208=SPHERICAL_SURFACE('',#10974,0.300000000000003);
#209=SPHERICAL_SURFACE('',#10978,0.299999999999994);
#210=SPHERICAL_SURFACE('',#10983,0.300000000000011);
#261=TOROIDAL_SURFACE('',#10928,4.79999999999999,0.3);
#262=TOROIDAL_SURFACE('',#10934,4.79999999999998,0.3);
#263=TOROIDAL_SURFACE('',#10941,0.600000000000001,0.3);
#264=TOROIDAL_SURFACE('',#10950,0.600000000000001,0.300000000000011);
#265=TOROIDAL_SURFACE('',#11013,4.79999999999998,0.3);
#266=TOROIDAL_SURFACE('',#11018,4.79999999999999,0.3);
#285=ELLIPSE('',#10956,0.424264068711946,0.3);
#286=ELLIPSE('',#11000,0.424264068711924,0.3);
#296=SHAPE_REPRESENTATION_RELATIONSHIP('SRR','None',#17883,#306);
#306=ADVANCED_BREP_SHAPE_REPRESENTATION('',(#326),#17835);
#316=STYLED_ITEM('',(#17987),#326);
#326=MANIFOLD_SOLID_BREP('Clamp_04',#9637);
#617=CYLINDRICAL_SURFACE('',#10925,0.3);
#618=CYLINDRICAL_SURFACE('',#10932,0.3);
#619=CYLINDRICAL_SURFACE('',#10937,4.49999999999999);
#620=CYLINDRICAL_SURFACE('',#10955,0.3);
#621=CYLINDRICAL_SURFACE('',#10965,0.3);
#622=CYLINDRICAL_SURFACE('',#10982,0.3);
#623=CYLINDRICAL_SURFACE('',#10987,0.3);
#624=CYLINDRICAL_SURFACE('',#10988,0.3);
#625=CYLINDRICAL_SURFACE('',#10989,0.3);
#626=CYLINDRICAL_SURFACE('',#10990,0.3);
#627=CYLINDRICAL_SURFACE('',#10991,0.3);
#628=CYLINDRICAL_SURFACE('',#10992,0.3);
#629=CYLINDRICAL_SURFACE('',#10993,0.3);
#630=CYLINDRICAL_SURFACE('',#10994,0.3);
#631=CYLINDRICAL_SURFACE('',#10995,0.3);
#632=CYLINDRICAL_SURFACE('',#10996,0.3);
#633=CYLINDRICAL_SURFACE('',#10997,0.3);
#634=CYLINDRICAL_SURFACE('',#10998,0.3);
#635=CYLINDRICAL_SURFACE('',#10999,0.3);
#636=CYLINDRICAL_SURFACE('',#11001,0.3);
#637=CYLINDRICAL_SURFACE('',#11010,0.3);
#638=CYLINDRICAL_SURFACE('',#11016,0.3);
#639=CYLINDRICAL_SURFACE('',#11019,4.49999999999998);
#1258=LINE('',#17612,#1923);
#1259=LINE('',#17615,#1924);
#1260=LINE('',#17626,#1925);
#1261=LINE('',#17627,#1926);
#1262=LINE('',#17633,#1927);
#1263=LINE('',#17636,#1928);
#1264=LINE('',#17639,#1929);
#1265=LINE('',#17640,#1930);
#1266=LINE('',#17644,#1931);
#1267=LINE('',#17646,#1932);
#1268=LINE('',#17648,#1933);
#1269=LINE('',#17649,#1934);
#1270=LINE('',#17675,#1935);
#1271=LINE('',#17677,#1936);
#1272=LINE('',#17693,#1937);
#1273=LINE('',#17694,#1938);
#1274=LINE('',#17723,#1939);
#1275=LINE('',#17724,#1940);
#1276=LINE('',#17733,#1941);
#1277=LINE('',#17734,#1942);
#1278=LINE('',#17736,#1943);
#1279=LINE('',#17737,#1944);
#1280=LINE('',#17739,#1945);
#1281=LINE('',#17740,#1946);
#1282=LINE('',#17742,#1947);
#1283=LINE('',#17743,#1948);
#1284=LINE('',#17745,#1949);
#1285=LINE('',#17746,#1950);
#1286=LINE('',#17748,#1951);
#1287=LINE('',#17749,#1952);
#1288=LINE('',#17751,#1953);
#1289=LINE('',#17753,#1954);
#1290=LINE('',#17755,#1955);
#1291=LINE('',#17756,#1956);
#1292=LINE('',#17758,#1957);
#1293=LINE('',#17759,#1958);
#1294=LINE('',#17761,#1959);
#1295=LINE('',#17763,#1960);
#1296=LINE('',#17766,#1961);
#1297=LINE('',#17768,#1962);
#1298=LINE('',#17771,#1963);
#1299=LINE('',#17772,#1964);
#1300=LINE('',#17774,#1965);
#1301=LINE('',#17780,#1966);
#1302=LINE('',#17784,#1967);
#1303=LINE('',#17797,#1968);
#1304=LINE('',#17800,#1969);
#1923=VECTOR('',#14006,10.);
#1924=VECTOR('',#14009,10.);
#1925=VECTOR('',#14022,10.);
#1926=VECTOR('',#14023,10.);
#1927=VECTOR('',#14032,10.);
#1928=VECTOR('',#14035,10.);
#1929=VECTOR('',#14038,10.);
#1930=VECTOR('',#14039,10.);
#1931=VECTOR('',#14042,10.);
#1932=VECTOR('',#14043,10.);
#1933=VECTOR('',#14044,10.);
#1934=VECTOR('',#14045,10.);
#1935=VECTOR('',#14076,10.);
#1936=VECTOR('',#14077,10.);
#1937=VECTOR('',#14098,10.);
#1938=VECTOR('',#14099,10.);
#1939=VECTOR('',#14134,10.);
#1940=VECTOR('',#14135,10.);
#1941=VECTOR('',#14146,10.);
#1942=VECTOR('',#14147,10.);
#1943=VECTOR('',#14150,10.);
#1944=VECTOR('',#14151,10.);
#1945=VECTOR('',#14154,10.);
#1946=VECTOR('',#14155,10.);
#1947=VECTOR('',#14158,10.);
#1948=VECTOR('',#14159,10.);
#1949=VECTOR('',#14162,10.);
#1950=VECTOR('',#14163,10.);
#1951=VECTOR('',#14166,10.);
#1952=VECTOR('',#14167,10.);
#1953=VECTOR('',#14170,10.);
#1954=VECTOR('',#14173,10.);
#1955=VECTOR('',#14176,10.);
#1956=VECTOR('',#14177,10.);
#1957=VECTOR('',#14180,10.);
#1958=VECTOR('',#14181,10.);
#1959=VECTOR('',#14184,10.);
#1960=VECTOR('',#14187,10.);
#1961=VECTOR('',#14190,10.);
#1962=VECTOR('',#14191,10.);
#1963=VECTOR('',#14196,10.);
#1964=VECTOR('',#14197,10.);
#1965=VECTOR('',#14200,10.);
#1966=VECTOR('',#14207,10.);
#1967=VECTOR('',#14210,10.);
#1968=VECTOR('',#14233,10.);
#1969=VECTOR('',#14238,10.);
#2025=FACE_BOUND('',#3266,.T.);
#2026=FACE_BOUND('',#3298,.T.);
#2594=FACE_OUTER_BOUND('',#3259,.T.);
#2595=FACE_OUTER_BOUND('',#3260,.T.);
#2596=FACE_OUTER_BOUND('',#3261,.T.);
#2597=FACE_OUTER_BOUND('',#3262,.T.);
#2598=FACE_OUTER_BOUND('',#3263,.T.);
#2599=FACE_OUTER_BOUND('',#3264,.T.);
#2600=FACE_OUTER_BOUND('',#3265,.T.);
#2601=FACE_OUTER_BOUND('',#3267,.T.);
#2602=FACE_OUTER_BOUND('',#3268,.T.);
#2603=FACE_OUTER_BOUND('',#3269,.T.);
#2604=FACE_OUTER_BOUND('',#3270,.T.);
#2605=FACE_OUTER_BOUND('',#3271,.T.);
#2606=FACE_OUTER_BOUND('',#3272,.T.);
#2607=FACE_OUTER_BOUND('',#3273,.T.);
#2608=FACE_OUTER_BOUND('',#3274,.T.);
#2609=FACE_OUTER_BOUND('',#3275,.T.);
#2610=FACE_OUTER_BOUND('',#3276,.T.);
#2611=FACE_OUTER_BOUND('',#3277,.T.);
#2612=FACE_OUTER_BOUND('',#3278,.T.);
#2613=FACE_OUTER_BOUND('',#3279,.T.);
#2614=FACE_OUTER_BOUND('',#3280,.T.);
#2615=FACE_OUTER_BOUND('',#3281,.T.);
#2616=FACE_OUTER_BOUND('',#3282,.T.);
#2617=FACE_OUTER_BOUND('',#3283,.T.);
#2618=FACE_OUTER_BOUND('',#3284,.T.);
#2619=FACE_OUTER_BOUND('',#3285,.T.);
#2620=FACE_OUTER_BOUND('',#3286,.T.);
#2621=FACE_OUTER_BOUND('',#3287,.T.);
#2622=FACE_OUTER_BOUND('',#3288,.T.);
#2623=FACE_OUTER_BOUND('',#3289,.T.);
#2624=FACE_OUTER_BOUND('',#3290,.T.);
#2625=FACE_OUTER_BOUND('',#3291,.T.);
#2626=FACE_OUTER_BOUND('',#3292,.T.);
#2627=FACE_OUTER_BOUND('',#3293,.T.);
#2628=FACE_OUTER_BOUND('',#3294,.T.);
#2629=FACE_OUTER_BOUND('',#3295,.T.);
#2630=FACE_OUTER_BOUND('',#3296,.T.);
#2631=FACE_OUTER_BOUND('',#3297,.T.);
#2632=FACE_OUTER_BOUND('',#3299,.T.);
#2633=FACE_OUTER_BOUND('',#3300,.T.);
#2634=FACE_OUTER_BOUND('',#3301,.T.);
#2635=FACE_OUTER_BOUND('',#3302,.T.);
#2636=FACE_OUTER_BOUND('',#3303,.T.);
#2637=FACE_OUTER_BOUND('',#3304,.T.);
#2638=FACE_OUTER_BOUND('',#3305,.T.);
#2639=FACE_OUTER_BOUND('',#3306,.T.);
#2640=FACE_OUTER_BOUND('',#3307,.T.);
#3259=EDGE_LOOP('',(#8671,#8672,#8673,#8674));
#3260=EDGE_LOOP('',(#8675,#8676,#8677,#8678));
#3261=EDGE_LOOP('',(#8679,#8680,#8681,#8682));
#3262=EDGE_LOOP('',(#8683,#8684,#8685,#8686));
#3263=EDGE_LOOP('',(#8687,#8688,#8689,#8690));
#3264=EDGE_LOOP('',(#8691,#8692,#8693,#8694));
#3265=EDGE_LOOP('',(#8695,#8696,#8697,#8698));
#3266=EDGE_LOOP('',(#8699,#8700,#8701,#8702));
#3267=EDGE_LOOP('',(#8703,#8704,#8705,#8706));
#3268=EDGE_LOOP('',(#8707,#8708,#8709));
#3269=EDGE_LOOP('',(#8710,#8711,#8712,#8713));
#3270=EDGE_LOOP('',(#8714,#8715,#8716,#8717));
#3271=EDGE_LOOP('',(#8718,#8719,#8720));
#3272=EDGE_LOOP('',(#8721,#8722,#8723));
#3273=EDGE_LOOP('',(#8724,#8725,#8726,#8727));
#3274=EDGE_LOOP('',(#8728,#8729,#8730));
#3275=EDGE_LOOP('',(#8731,#8732,#8733));
#3276=EDGE_LOOP('',(#8734,#8735,#8736));
#3277=EDGE_LOOP('',(#8737,#8738,#8739));
#3278=EDGE_LOOP('',(#8740,#8741,#8742,#8743));
#3279=EDGE_LOOP('',(#8744,#8745,#8746));
#3280=EDGE_LOOP('',(#8747,#8748,#8749,#8750));
#3281=EDGE_LOOP('',(#8751,#8752,#8753,#8754));
#3282=EDGE_LOOP('',(#8755,#8756,#8757,#8758));
#3283=EDGE_LOOP('',(#8759,#8760,#8761,#8762));
#3284=EDGE_LOOP('',(#8763,#8764,#8765,#8766));
#3285=EDGE_LOOP('',(#8767,#8768,#8769,#8770));
#3286=EDGE_LOOP('',(#8771,#8772,#8773,#8774));
#3287=EDGE_LOOP('',(#8775,#8776,#8777,#8778));
#3288=EDGE_LOOP('',(#8779,#8780,#8781,#8782));
#3289=EDGE_LOOP('',(#8783,#8784,#8785,#8786));
#3290=EDGE_LOOP('',(#8787,#8788,#8789,#8790));
#3291=EDGE_LOOP('',(#8791,#8792,#8793,#8794));
#3292=EDGE_LOOP('',(#8795,#8796,#8797,#8798));
#3293=EDGE_LOOP('',(#8799,#8800,#8801,#8802));
#3294=EDGE_LOOP('',(#8803,#8804,#8805,#8806));
#3295=EDGE_LOOP('',(#8807,#8808,#8809,#8810,#8811,#8812,#8813));
#3296=EDGE_LOOP('',(#8814,#8815,#8816,#8817));
#3297=EDGE_LOOP('',(#8818,#8819,#8820,#8821));
#3298=EDGE_LOOP('',(#8822,#8823,#8824,#8825));
#3299=EDGE_LOOP('',(#8826,#8827,#8828,#8829));
#3300=EDGE_LOOP('',(#8830,#8831,#8832,#8833,#8834,#8835,#8836));
#3301=EDGE_LOOP('',(#8837,#8838,#8839,#8840));
#3302=EDGE_LOOP('',(#8841,#8842,#8843,#8844));
#3303=EDGE_LOOP('',(#8845,#8846,#8847,#8848));
#3304=EDGE_LOOP('',(#8849,#8850,#8851,#8852));
#3305=EDGE_LOOP('',(#8853,#8854,#8855,#8856));
#3306=EDGE_LOOP('',(#8857,#8858,#8859,#8860));
#3307=EDGE_LOOP('',(#8861,#8862,#8863,#8864));
#3888=CIRCLE('',#10926,0.3);
#3889=CIRCLE('',#10927,0.299999999999994);
#3890=CIRCLE('',#10929,0.300000000000011);
#3891=CIRCLE('',#10930,4.79999999999999);
#3892=CIRCLE('',#10931,4.49999999999999);
#3893=CIRCLE('',#10933,0.300000000000002);
#3894=CIRCLE('',#10935,4.79999999999998);
#3895=CIRCLE('',#10936,4.49999999999998);
#3896=CIRCLE('',#10938,4.49999999999999);
#3897=CIRCLE('',#10942,0.3);
#3898=CIRCLE('',#10943,0.299999999999994);
#3899=CIRCLE('',#10944,0.300000000000011);
#3900=CIRCLE('',#10945,0.599999999999987);
#3901=CIRCLE('',#10947,0.3);
#3902=CIRCLE('',#10948,0.299999999999994);
#3903=CIRCLE('',#10949,0.300000000000011);
#3904=CIRCLE('',#10951,0.600000000000001);
#3905=CIRCLE('',#10952,0.299999999999976);
#3906=CIRCLE('',#10953,0.3);
#3907=CIRCLE('',#10954,0.300000000000011);
#3908=CIRCLE('',#10958,0.300000000000003);
#3909=CIRCLE('',#10959,0.3);
#3910=CIRCLE('',#10960,0.300000000000011);
#3911=CIRCLE('',#10962,0.3);
#3912=CIRCLE('',#10963,0.299999999999994);
#3913=CIRCLE('',#10964,0.300000000000011);
#3914=CIRCLE('',#10967,0.299999999999994);
#3915=CIRCLE('',#10968,0.3);
#3916=CIRCLE('',#10969,0.300000000000011);
#3917=CIRCLE('',#10971,0.300000000000006);
#3918=CIRCLE('',#10972,0.300000000000011);
#3919=CIRCLE('',#10973,0.3);
#3920=CIRCLE('',#10975,0.3);
#3921=CIRCLE('',#10976,0.300000000000003);
#3922=CIRCLE('',#10977,0.300000000000011);
#3923=CIRCLE('',#10979,0.300000000000011);
#3924=CIRCLE('',#10980,0.299999999999994);
#3925=CIRCLE('',#10981,0.3);
#3926=CIRCLE('',#10984,0.3);
#3927=CIRCLE('',#10985,0.300000000000011);
#3928=CIRCLE('',#10986,0.300000000000001);
#3929=CIRCLE('',#11006,4.79999999999998);
#3930=CIRCLE('',#11007,4.79999999999999);
#3931=CIRCLE('',#11011,0.3);
#3932=CIRCLE('',#11012,0.299999999999994);
#3933=CIRCLE('',#11014,0.300000000000002);
#3934=CIRCLE('',#11015,4.49999999999998);
#3935=CIRCLE('',#11017,0.300000000000002);
#4670=VERTEX_POINT('',#17608);
#4671=VERTEX_POINT('',#17609);
#4672=VERTEX_POINT('',#17611);
#4673=VERTEX_POINT('',#17613);
#4674=VERTEX_POINT('',#17617);
#4675=VERTEX_POINT('',#17618);
#4676=VERTEX_POINT('',#17623);
#4677=VERTEX_POINT('',#17624);
#4678=VERTEX_POINT('',#17632);
#4679=VERTEX_POINT('',#17634);
#4680=VERTEX_POINT('',#17638);
#4681=VERTEX_POINT('',#17642);
#4682=VERTEX_POINT('',#17643);
#4683=VERTEX_POINT('',#17645);
#4684=VERTEX_POINT('',#17647);
#4685=VERTEX_POINT('',#17651);
#4686=VERTEX_POINT('',#17653);
#4687=VERTEX_POINT('',#17655);
#4688=VERTEX_POINT('',#17659);
#4689=VERTEX_POINT('',#17660);
#4690=VERTEX_POINT('',#17662);
#4691=VERTEX_POINT('',#17666);
#4692=VERTEX_POINT('',#17667);
#4693=VERTEX_POINT('',#17669);
#4694=VERTEX_POINT('',#17674);
#4695=VERTEX_POINT('',#17676);
#4696=VERTEX_POINT('',#17680);
#4697=VERTEX_POINT('',#17681);
#4698=VERTEX_POINT('',#17686);
#4699=VERTEX_POINT('',#17687);
#4700=VERTEX_POINT('',#17689);
#4701=VERTEX_POINT('',#17696);
#4702=VERTEX_POINT('',#17697);
#4703=VERTEX_POINT('',#17699);
#4704=VERTEX_POINT('',#17703);
#4705=VERTEX_POINT('',#17705);
#4706=VERTEX_POINT('',#17709);
#4707=VERTEX_POINT('',#17710);
#4708=VERTEX_POINT('',#17712);
#4709=VERTEX_POINT('',#17716);
#4710=VERTEX_POINT('',#17717);
#4711=VERTEX_POINT('',#17719);
#4712=VERTEX_POINT('',#17726);
#4713=VERTEX_POINT('',#17727);
#4714=VERTEX_POINT('',#17729);
#4715=VERTEX_POINT('',#17765);
#4716=VERTEX_POINT('',#17767);
#4717=VERTEX_POINT('',#17778);
#4718=VERTEX_POINT('',#17779);
#4719=VERTEX_POINT('',#17781);
#4720=VERTEX_POINT('',#17783);
#4721=VERTEX_POINT('',#17792);
#6006=EDGE_CURVE('',#4670,#4671,#3888,.T.);
#6007=EDGE_CURVE('',#4671,#4672,#1258,.T.);
#6008=EDGE_CURVE('',#4672,#4673,#3889,.T.);
#6009=EDGE_CURVE('',#4673,#4670,#1259,.T.);
#6010=EDGE_CURVE('',#4674,#4675,#3890,.T.);
#6011=EDGE_CURVE('',#4675,#4673,#3891,.T.);
#6012=EDGE_CURVE('',#4672,#4674,#3892,.T.);
#6013=EDGE_CURVE('',#4676,#4677,#3893,.T.);
#6014=EDGE_CURVE('',#4677,#4675,#1260,.T.);
#6015=EDGE_CURVE('',#4674,#4676,#1261,.T.);
#6016=EDGE_CURVE('',#4670,#4677,#3894,.T.);
#6017=EDGE_CURVE('',#4676,#4671,#3895,.T.);
#6018=EDGE_CURVE('',#4678,#4672,#1262,.T.);
#6019=EDGE_CURVE('',#4679,#4678,#3896,.T.);
#6020=EDGE_CURVE('',#4679,#4674,#1263,.T.);
#6021=EDGE_CURVE('',#4680,#4671,#1264,.T.);
#6022=EDGE_CURVE('',#4678,#4680,#1265,.T.);
#6023=EDGE_CURVE('',#4681,#4682,#1266,.T.);
#6024=EDGE_CURVE('',#4683,#4681,#1267,.T.);
#6025=EDGE_CURVE('',#4684,#4683,#1268,.T.);
#6026=EDGE_CURVE('',#4682,#4684,#1269,.T.);
#6027=EDGE_CURVE('',#4683,#4685,#3897,.T.);
#6028=EDGE_CURVE('',#4686,#4683,#3898,.F.);
#6029=EDGE_CURVE('',#4687,#4686,#3899,.T.);
#6030=EDGE_CURVE('',#4687,#4685,#3900,.T.);
#6031=EDGE_CURVE('',#4688,#4689,#3901,.F.);
#6032=EDGE_CURVE('',#4690,#4688,#3902,.F.);
#6033=EDGE_CURVE('',#4689,#4690,#3903,.F.);
#6034=EDGE_CURVE('',#4691,#4692,#3904,.T.);
#6035=EDGE_CURVE('',#4693,#4692,#3905,.T.);
#6036=EDGE_CURVE('',#4681,#4693,#3906,.F.);
#6037=EDGE_CURVE('',#4691,#4681,#3907,.T.);
#6038=EDGE_CURVE('',#4694,#4693,#1270,.T.);
#6039=EDGE_CURVE('',#4692,#4695,#1271,.T.);
#6040=EDGE_CURVE('',#4695,#4694,#285,.T.);
#6041=EDGE_CURVE('',#4696,#4697,#3908,.F.);
#6042=EDGE_CURVE('',#4684,#4696,#3909,.F.);
#6043=EDGE_CURVE('',#4697,#4684,#3910,.F.);
#6044=EDGE_CURVE('',#4698,#4699,#3911,.F.);
#6045=EDGE_CURVE('',#4700,#4698,#3912,.F.);
#6046=EDGE_CURVE('',#4699,#4700,#3913,.F.);
#6047=EDGE_CURVE('',#4695,#4700,#1272,.T.);
#6048=EDGE_CURVE('',#4698,#4694,#1273,.T.);
#6049=EDGE_CURVE('',#4701,#4702,#3914,.F.);
#6050=EDGE_CURVE('',#4703,#4701,#3915,.F.);
#6051=EDGE_CURVE('',#4702,#4703,#3916,.F.);
#6052=EDGE_CURVE('',#4704,#4682,#3917,.F.);
#6053=EDGE_CURVE('',#4705,#4704,#3918,.F.);
#6054=EDGE_CURVE('',#4682,#4705,#3919,.F.);
#6055=EDGE_CURVE('',#4706,#4707,#3920,.F.);
#6056=EDGE_CURVE('',#4708,#4706,#3921,.F.);
#6057=EDGE_CURVE('',#4707,#4708,#3922,.F.);
#6058=EDGE_CURVE('',#4709,#4710,#3923,.F.);
#6059=EDGE_CURVE('',#4711,#4709,#3924,.F.);
#6060=EDGE_CURVE('',#4710,#4711,#3925,.F.);
#6061=EDGE_CURVE('',#4709,#4699,#1274,.T.);
#6062=EDGE_CURVE('',#4700,#4711,#1275,.T.);
#6063=EDGE_CURVE('',#4712,#4713,#3926,.F.);
#6064=EDGE_CURVE('',#4714,#4712,#3927,.F.);
#6065=EDGE_CURVE('',#4713,#4714,#3928,.F.);
#6066=EDGE_CURVE('',#4711,#4714,#1276,.T.);
#6067=EDGE_CURVE('',#4712,#4710,#1277,.T.);
#6068=EDGE_CURVE('',#4714,#4705,#1278,.T.);
#6069=EDGE_CURVE('',#4704,#4713,#1279,.T.);
#6070=EDGE_CURVE('',#4706,#4712,#1280,.T.);
#6071=EDGE_CURVE('',#4713,#4708,#1281,.T.);
#6072=EDGE_CURVE('',#4701,#4709,#1282,.T.);
#6073=EDGE_CURVE('',#4710,#4703,#1283,.T.);
#6074=EDGE_CURVE('',#4697,#4707,#1284,.T.);
#6075=EDGE_CURVE('',#4708,#4696,#1285,.T.);
#6076=EDGE_CURVE('',#4707,#4702,#1286,.T.);
#6077=EDGE_CURVE('',#4703,#4706,#1287,.T.);
#6078=EDGE_CURVE('',#4705,#4691,#1288,.T.);
#6079=EDGE_CURVE('',#4696,#4704,#1289,.T.);
#6080=EDGE_CURVE('',#4702,#4689,#1290,.T.);
#6081=EDGE_CURVE('',#4690,#4701,#1291,.T.);
#6082=EDGE_CURVE('',#4688,#4698,#1292,.T.);
#6083=EDGE_CURVE('',#4699,#4690,#1293,.T.);
#6084=EDGE_CURVE('',#4685,#4697,#1294,.T.);
#6085=EDGE_CURVE('',#4693,#4686,#1295,.T.);
#6086=EDGE_CURVE('',#4715,#4688,#1296,.T.);
#6087=EDGE_CURVE('',#4689,#4716,#1297,.T.);
#6088=EDGE_CURVE('',#4716,#4715,#286,.T.);
#6089=EDGE_CURVE('',#4716,#4687,#1298,.T.);
#6090=EDGE_CURVE('',#4686,#4715,#1299,.T.);
#6091=EDGE_CURVE('',#4694,#4715,#1300,.T.);
#6092=EDGE_CURVE('',#4717,#4718,#1301,.T.);
#6093=EDGE_CURVE('',#4719,#4717,#3929,.T.);
#6094=EDGE_CURVE('',#4720,#4719,#1302,.T.);
#6095=EDGE_CURVE('',#4718,#4720,#3930,.T.);
#6096=EDGE_CURVE('',#4718,#4678,#3931,.T.);
#6097=EDGE_CURVE('',#4680,#4717,#3932,.T.);
#6098=EDGE_CURVE('',#4721,#4719,#3933,.T.);
#6099=EDGE_CURVE('',#4680,#4721,#3934,.T.);
#6100=EDGE_CURVE('',#4679,#4720,#3935,.T.);
#6101=EDGE_CURVE('',#4721,#4679,#1303,.T.);
#6102=EDGE_CURVE('',#4721,#4676,#1304,.T.);
#8671=ORIENTED_EDGE('',*,*,#6006,.T.);
#8672=ORIENTED_EDGE('',*,*,#6007,.T.);
#8673=ORIENTED_EDGE('',*,*,#6008,.T.);
#8674=ORIENTED_EDGE('',*,*,#6009,.T.);
#8675=ORIENTED_EDGE('',*,*,#6010,.T.);
#8676=ORIENTED_EDGE('',*,*,#6011,.T.);
#8677=ORIENTED_EDGE('',*,*,#6008,.F.);
#8678=ORIENTED_EDGE('',*,*,#6012,.T.);
#8679=ORIENTED_EDGE('',*,*,#6013,.T.);
#8680=ORIENTED_EDGE('',*,*,#6014,.T.);
#8681=ORIENTED_EDGE('',*,*,#6010,.F.);
#8682=ORIENTED_EDGE('',*,*,#6015,.T.);
#8683=ORIENTED_EDGE('',*,*,#6006,.F.);
#8684=ORIENTED_EDGE('',*,*,#6016,.T.);
#8685=ORIENTED_EDGE('',*,*,#6013,.F.);
#8686=ORIENTED_EDGE('',*,*,#6017,.T.);
#8687=ORIENTED_EDGE('',*,*,#6012,.F.);
#8688=ORIENTED_EDGE('',*,*,#6018,.F.);
#8689=ORIENTED_EDGE('',*,*,#6019,.F.);
#8690=ORIENTED_EDGE('',*,*,#6020,.T.);
#8691=ORIENTED_EDGE('',*,*,#6007,.F.);
#8692=ORIENTED_EDGE('',*,*,#6021,.F.);
#8693=ORIENTED_EDGE('',*,*,#6022,.F.);
#8694=ORIENTED_EDGE('',*,*,#6018,.T.);
#8695=ORIENTED_EDGE('',*,*,#6023,.F.);
#8696=ORIENTED_EDGE('',*,*,#6024,.F.);
#8697=ORIENTED_EDGE('',*,*,#6025,.F.);
#8698=ORIENTED_EDGE('',*,*,#6026,.F.);
#8699=ORIENTED_EDGE('',*,*,#6009,.F.);
#8700=ORIENTED_EDGE('',*,*,#6011,.F.);
#8701=ORIENTED_EDGE('',*,*,#6014,.F.);
#8702=ORIENTED_EDGE('',*,*,#6016,.F.);
#8703=ORIENTED_EDGE('',*,*,#6027,.F.);
#8704=ORIENTED_EDGE('',*,*,#6028,.F.);
#8705=ORIENTED_EDGE('',*,*,#6029,.F.);
#8706=ORIENTED_EDGE('',*,*,#6030,.T.);
#8707=ORIENTED_EDGE('',*,*,#6031,.F.);
#8708=ORIENTED_EDGE('',*,*,#6032,.F.);
#8709=ORIENTED_EDGE('',*,*,#6033,.F.);
#8710=ORIENTED_EDGE('',*,*,#6034,.T.);
#8711=ORIENTED_EDGE('',*,*,#6035,.F.);
#8712=ORIENTED_EDGE('',*,*,#6036,.F.);
#8713=ORIENTED_EDGE('',*,*,#6037,.F.);
#8714=ORIENTED_EDGE('',*,*,#6038,.T.);
#8715=ORIENTED_EDGE('',*,*,#6035,.T.);
#8716=ORIENTED_EDGE('',*,*,#6039,.T.);
#8717=ORIENTED_EDGE('',*,*,#6040,.T.);
#8718=ORIENTED_EDGE('',*,*,#6041,.F.);
#8719=ORIENTED_EDGE('',*,*,#6042,.F.);
#8720=ORIENTED_EDGE('',*,*,#6043,.F.);
#8721=ORIENTED_EDGE('',*,*,#6044,.F.);
#8722=ORIENTED_EDGE('',*,*,#6045,.F.);
#8723=ORIENTED_EDGE('',*,*,#6046,.F.);
#8724=ORIENTED_EDGE('',*,*,#6047,.T.);
#8725=ORIENTED_EDGE('',*,*,#6045,.T.);
#8726=ORIENTED_EDGE('',*,*,#6048,.T.);
#8727=ORIENTED_EDGE('',*,*,#6040,.F.);
#8728=ORIENTED_EDGE('',*,*,#6049,.F.);
#8729=ORIENTED_EDGE('',*,*,#6050,.F.);
#8730=ORIENTED_EDGE('',*,*,#6051,.F.);
#8731=ORIENTED_EDGE('',*,*,#6052,.F.);
#8732=ORIENTED_EDGE('',*,*,#6053,.F.);
#8733=ORIENTED_EDGE('',*,*,#6054,.F.);
#8734=ORIENTED_EDGE('',*,*,#6055,.F.);
#8735=ORIENTED_EDGE('',*,*,#6056,.F.);
#8736=ORIENTED_EDGE('',*,*,#6057,.F.);
#8737=ORIENTED_EDGE('',*,*,#6058,.F.);
#8738=ORIENTED_EDGE('',*,*,#6059,.F.);
#8739=ORIENTED_EDGE('',*,*,#6060,.F.);
#8740=ORIENTED_EDGE('',*,*,#6059,.T.);
#8741=ORIENTED_EDGE('',*,*,#6061,.T.);
#8742=ORIENTED_EDGE('',*,*,#6046,.T.);
#8743=ORIENTED_EDGE('',*,*,#6062,.T.);
#8744=ORIENTED_EDGE('',*,*,#6063,.F.);
#8745=ORIENTED_EDGE('',*,*,#6064,.F.);
#8746=ORIENTED_EDGE('',*,*,#6065,.F.);
#8747=ORIENTED_EDGE('',*,*,#6060,.T.);
#8748=ORIENTED_EDGE('',*,*,#6066,.T.);
#8749=ORIENTED_EDGE('',*,*,#6064,.T.);
#8750=ORIENTED_EDGE('',*,*,#6067,.T.);
#8751=ORIENTED_EDGE('',*,*,#6065,.T.);
#8752=ORIENTED_EDGE('',*,*,#6068,.T.);
#8753=ORIENTED_EDGE('',*,*,#6053,.T.);
#8754=ORIENTED_EDGE('',*,*,#6069,.T.);
#8755=ORIENTED_EDGE('',*,*,#6056,.T.);
#8756=ORIENTED_EDGE('',*,*,#6070,.T.);
#8757=ORIENTED_EDGE('',*,*,#6063,.T.);
#8758=ORIENTED_EDGE('',*,*,#6071,.T.);
#8759=ORIENTED_EDGE('',*,*,#6050,.T.);
#8760=ORIENTED_EDGE('',*,*,#6072,.T.);
#8761=ORIENTED_EDGE('',*,*,#6058,.T.);
#8762=ORIENTED_EDGE('',*,*,#6073,.T.);
#8763=ORIENTED_EDGE('',*,*,#6041,.T.);
#8764=ORIENTED_EDGE('',*,*,#6074,.T.);
#8765=ORIENTED_EDGE('',*,*,#6057,.T.);
#8766=ORIENTED_EDGE('',*,*,#6075,.T.);
#8767=ORIENTED_EDGE('',*,*,#6055,.T.);
#8768=ORIENTED_EDGE('',*,*,#6076,.T.);
#8769=ORIENTED_EDGE('',*,*,#6051,.T.);
#8770=ORIENTED_EDGE('',*,*,#6077,.T.);
#8771=ORIENTED_EDGE('',*,*,#6054,.T.);
#8772=ORIENTED_EDGE('',*,*,#6078,.T.);
#8773=ORIENTED_EDGE('',*,*,#6037,.T.);
#8774=ORIENTED_EDGE('',*,*,#6023,.T.);
#8775=ORIENTED_EDGE('',*,*,#6042,.T.);
#8776=ORIENTED_EDGE('',*,*,#6079,.T.);
#8777=ORIENTED_EDGE('',*,*,#6052,.T.);
#8778=ORIENTED_EDGE('',*,*,#6026,.T.);
#8779=ORIENTED_EDGE('',*,*,#6049,.T.);
#8780=ORIENTED_EDGE('',*,*,#6080,.T.);
#8781=ORIENTED_EDGE('',*,*,#6033,.T.);
#8782=ORIENTED_EDGE('',*,*,#6081,.T.);
#8783=ORIENTED_EDGE('',*,*,#6032,.T.);
#8784=ORIENTED_EDGE('',*,*,#6082,.T.);
#8785=ORIENTED_EDGE('',*,*,#6044,.T.);
#8786=ORIENTED_EDGE('',*,*,#6083,.T.);
#8787=ORIENTED_EDGE('',*,*,#6027,.T.);
#8788=ORIENTED_EDGE('',*,*,#6084,.T.);
#8789=ORIENTED_EDGE('',*,*,#6043,.T.);
#8790=ORIENTED_EDGE('',*,*,#6025,.T.);
#8791=ORIENTED_EDGE('',*,*,#6028,.T.);
#8792=ORIENTED_EDGE('',*,*,#6024,.T.);
#8793=ORIENTED_EDGE('',*,*,#6036,.T.);
#8794=ORIENTED_EDGE('',*,*,#6085,.T.);
#8795=ORIENTED_EDGE('',*,*,#6086,.T.);
#8796=ORIENTED_EDGE('',*,*,#6031,.T.);
#8797=ORIENTED_EDGE('',*,*,#6087,.T.);
#8798=ORIENTED_EDGE('',*,*,#6088,.T.);
#8799=ORIENTED_EDGE('',*,*,#6089,.T.);
#8800=ORIENTED_EDGE('',*,*,#6029,.T.);
#8801=ORIENTED_EDGE('',*,*,#6090,.T.);
#8802=ORIENTED_EDGE('',*,*,#6088,.F.);
#8803=ORIENTED_EDGE('',*,*,#6090,.F.);
#8804=ORIENTED_EDGE('',*,*,#6085,.F.);
#8805=ORIENTED_EDGE('',*,*,#6038,.F.);
#8806=ORIENTED_EDGE('',*,*,#6091,.T.);
#8807=ORIENTED_EDGE('',*,*,#6034,.F.);
#8808=ORIENTED_EDGE('',*,*,#6078,.F.);
#8809=ORIENTED_EDGE('',*,*,#6068,.F.);
#8810=ORIENTED_EDGE('',*,*,#6066,.F.);
#8811=ORIENTED_EDGE('',*,*,#6062,.F.);
#8812=ORIENTED_EDGE('',*,*,#6047,.F.);
#8813=ORIENTED_EDGE('',*,*,#6039,.F.);
#8814=ORIENTED_EDGE('',*,*,#6061,.F.);
#8815=ORIENTED_EDGE('',*,*,#6072,.F.);
#8816=ORIENTED_EDGE('',*,*,#6081,.F.);
#8817=ORIENTED_EDGE('',*,*,#6083,.F.);
#8818=ORIENTED_EDGE('',*,*,#6067,.F.);
#8819=ORIENTED_EDGE('',*,*,#6070,.F.);
#8820=ORIENTED_EDGE('',*,*,#6077,.F.);
#8821=ORIENTED_EDGE('',*,*,#6073,.F.);
#8822=ORIENTED_EDGE('',*,*,#6092,.F.);
#8823=ORIENTED_EDGE('',*,*,#6093,.F.);
#8824=ORIENTED_EDGE('',*,*,#6094,.F.);
#8825=ORIENTED_EDGE('',*,*,#6095,.F.);
#8826=ORIENTED_EDGE('',*,*,#6069,.F.);
#8827=ORIENTED_EDGE('',*,*,#6079,.F.);
#8828=ORIENTED_EDGE('',*,*,#6075,.F.);
#8829=ORIENTED_EDGE('',*,*,#6071,.F.);
#8830=ORIENTED_EDGE('',*,*,#6074,.F.);
#8831=ORIENTED_EDGE('',*,*,#6084,.F.);
#8832=ORIENTED_EDGE('',*,*,#6030,.F.);
#8833=ORIENTED_EDGE('',*,*,#6089,.F.);
#8834=ORIENTED_EDGE('',*,*,#6087,.F.);
#8835=ORIENTED_EDGE('',*,*,#6080,.F.);
#8836=ORIENTED_EDGE('',*,*,#6076,.F.);
#8837=ORIENTED_EDGE('',*,*,#6096,.T.);
#8838=ORIENTED_EDGE('',*,*,#6022,.T.);
#8839=ORIENTED_EDGE('',*,*,#6097,.T.);
#8840=ORIENTED_EDGE('',*,*,#6092,.T.);
#8841=ORIENTED_EDGE('',*,*,#6098,.T.);
#8842=ORIENTED_EDGE('',*,*,#6093,.T.);
#8843=ORIENTED_EDGE('',*,*,#6097,.F.);
#8844=ORIENTED_EDGE('',*,*,#6099,.T.);
#8845=ORIENTED_EDGE('',*,*,#6100,.T.);
#8846=ORIENTED_EDGE('',*,*,#6094,.T.);
#8847=ORIENTED_EDGE('',*,*,#6098,.F.);
#8848=ORIENTED_EDGE('',*,*,#6101,.T.);
#8849=ORIENTED_EDGE('',*,*,#6096,.F.);
#8850=ORIENTED_EDGE('',*,*,#6095,.T.);
#8851=ORIENTED_EDGE('',*,*,#6100,.F.);
#8852=ORIENTED_EDGE('',*,*,#6019,.T.);
#8853=ORIENTED_EDGE('',*,*,#6017,.F.);
#8854=ORIENTED_EDGE('',*,*,#6102,.F.);
#8855=ORIENTED_EDGE('',*,*,#6099,.F.);
#8856=ORIENTED_EDGE('',*,*,#6021,.T.);
#8857=ORIENTED_EDGE('',*,*,#6015,.F.);
#8858=ORIENTED_EDGE('',*,*,#6020,.F.);
#8859=ORIENTED_EDGE('',*,*,#6101,.F.);
#8860=ORIENTED_EDGE('',*,*,#6102,.T.);
#8861=ORIENTED_EDGE('',*,*,#6086,.F.);
#8862=ORIENTED_EDGE('',*,*,#6091,.F.);
#8863=ORIENTED_EDGE('',*,*,#6048,.F.);
#8864=ORIENTED_EDGE('',*,*,#6082,.F.);
#9004=PLANE('',#10939);
#9005=PLANE('',#10940);
#9006=PLANE('',#11002);
#9007=PLANE('',#11003);
#9008=PLANE('',#11004);
#9009=PLANE('',#11005);
#9010=PLANE('',#11008);
#9011=PLANE('',#11009);
#9012=PLANE('',#11020);
#9013=PLANE('',#11021);
#9581=ADVANCED_FACE('',(#2594),#617,.T.);
#9582=ADVANCED_FACE('',(#2595),#261,.T.);
#9583=ADVANCED_FACE('',(#2596),#618,.T.);
#9584=ADVANCED_FACE('',(#2597),#262,.T.);
#9585=ADVANCED_FACE('',(#2598),#619,.F.);
#9586=ADVANCED_FACE('',(#2599),#9004,.F.);
#9587=ADVANCED_FACE('',(#2600,#2025),#9005,.T.);
#9588=ADVANCED_FACE('',(#2601),#263,.T.);
#9589=ADVANCED_FACE('',(#2602),#203,.T.);
#9590=ADVANCED_FACE('',(#2603),#264,.T.);
#9591=ADVANCED_FACE('',(#2604),#620,.T.);
#9592=ADVANCED_FACE('',(#2605),#204,.T.);
#9593=ADVANCED_FACE('',(#2606),#205,.T.);
#9594=ADVANCED_FACE('',(#2607),#621,.T.);
#9595=ADVANCED_FACE('',(#2608),#206,.T.);
#9596=ADVANCED_FACE('',(#2609),#207,.T.);
#9597=ADVANCED_FACE('',(#2610),#208,.T.);
#9598=ADVANCED_FACE('',(#2611),#209,.T.);
#9599=ADVANCED_FACE('',(#2612),#622,.T.);
#9600=ADVANCED_FACE('',(#2613),#210,.T.);
#9601=ADVANCED_FACE('',(#2614),#623,.T.);
#9602=ADVANCED_FACE('',(#2615),#624,.T.);
#9603=ADVANCED_FACE('',(#2616),#625,.T.);
#9604=ADVANCED_FACE('',(#2617),#626,.T.);
#9605=ADVANCED_FACE('',(#2618),#627,.T.);
#9606=ADVANCED_FACE('',(#2619),#628,.T.);
#9607=ADVANCED_FACE('',(#2620),#629,.T.);
#9608=ADVANCED_FACE('',(#2621),#630,.T.);
#9609=ADVANCED_FACE('',(#2622),#631,.T.);
#9610=ADVANCED_FACE('',(#2623),#632,.T.);
#9611=ADVANCED_FACE('',(#2624),#633,.T.);
#9612=ADVANCED_FACE('',(#2625),#634,.F.);
#9613=ADVANCED_FACE('',(#2626),#635,.T.);
#9614=ADVANCED_FACE('',(#2627),#636,.T.);
#9615=ADVANCED_FACE('',(#2628),#9006,.T.);
#9616=ADVANCED_FACE('',(#2629),#9007,.F.);
#9617=ADVANCED_FACE('',(#2630),#9008,.T.);
#9618=ADVANCED_FACE('',(#2631,#2026),#9009,.T.);
#9619=ADVANCED_FACE('',(#2632),#9010,.T.);
#9620=ADVANCED_FACE('',(#2633),#9011,.T.);
#9621=ADVANCED_FACE('',(#2634),#637,.T.);
#9622=ADVANCED_FACE('',(#2635),#265,.T.);
#9623=ADVANCED_FACE('',(#2636),#638,.T.);
#9624=ADVANCED_FACE('',(#2637),#266,.T.);
#9625=ADVANCED_FACE('',(#2638),#639,.F.);
#9626=ADVANCED_FACE('',(#2639),#9012,.F.);
#9627=ADVANCED_FACE('',(#2640),#9013,.T.);
#9637=CLOSED_SHELL('',(#9581,#9582,#9583,#9584,#9585,#9586,#9587,#9588,
#9589,#9590,#9591,#9592,#9593,#9594,#9595,#9596,#9597,#9598,#9599,#9600,
#9601,#9602,#9603,#9604,#9605,#9606,#9607,#9608,#9609,#9610,#9611,#9612,
#9613,#9614,#9615,#9616,#9617,#9618,#9619,#9620,#9621,#9622,#9623,#9624,
#9625,#9626,#9627));
#10924=AXIS2_PLACEMENT_3D('',#17606,#14000,#14001);
#10925=AXIS2_PLACEMENT_3D('',#17607,#14002,#14003);
#10926=AXIS2_PLACEMENT_3D('',#17610,#14004,#14005);
#10927=AXIS2_PLACEMENT_3D('',#17614,#14007,#14008);
#10928=AXIS2_PLACEMENT_3D('',#17616,#14010,#14011);
#10929=AXIS2_PLACEMENT_3D('',#17619,#14012,#14013);
#10930=AXIS2_PLACEMENT_3D('',#17620,#14014,#14015);
#10931=AXIS2_PLACEMENT_3D('',#17621,#14016,#14017);
#10932=AXIS2_PLACEMENT_3D('',#17622,#14018,#14019);
#10933=AXIS2_PLACEMENT_3D('',#17625,#14020,#14021);
#10934=AXIS2_PLACEMENT_3D('',#17628,#14024,#14025);
#10935=AXIS2_PLACEMENT_3D('',#17629,#14026,#14027);
#10936=AXIS2_PLACEMENT_3D('',#17630,#14028,#14029);
#10937=AXIS2_PLACEMENT_3D('',#17631,#14030,#14031);
#10938=AXIS2_PLACEMENT_3D('',#17635,#14033,#14034);
#10939=AXIS2_PLACEMENT_3D('',#17637,#14036,#14037);
#10940=AXIS2_PLACEMENT_3D('',#17641,#14040,#14041);
#10941=AXIS2_PLACEMENT_3D('',#17650,#14046,#14047);
#10942=AXIS2_PLACEMENT_3D('',#17652,#14048,#14049);
#10943=AXIS2_PLACEMENT_3D('',#17654,#14050,#14051);
#10944=AXIS2_PLACEMENT_3D('',#17656,#14052,#14053);
#10945=AXIS2_PLACEMENT_3D('',#17657,#14054,#14055);
#10946=AXIS2_PLACEMENT_3D('',#17658,#14056,#14057);
#10947=AXIS2_PLACEMENT_3D('',#17661,#14058,#14059);
#10948=AXIS2_PLACEMENT_3D('',#17663,#14060,#14061);
#10949=AXIS2_PLACEMENT_3D('',#17664,#14062,#14063);
#10950=AXIS2_PLACEMENT_3D('',#17665,#14064,#14065);
#10951=AXIS2_PLACEMENT_3D('',#17668,#14066,#14067);
#10952=AXIS2_PLACEMENT_3D('',#17670,#14068,#14069);
#10953=AXIS2_PLACEMENT_3D('',#17671,#14070,#14071);
#10954=AXIS2_PLACEMENT_3D('',#17672,#14072,#14073);
#10955=AXIS2_PLACEMENT_3D('',#17673,#14074,#14075);
#10956=AXIS2_PLACEMENT_3D('',#17678,#14078,#14079);
#10957=AXIS2_PLACEMENT_3D('',#17679,#14080,#14081);
#10958=AXIS2_PLACEMENT_3D('',#17682,#14082,#14083);
#10959=AXIS2_PLACEMENT_3D('',#17683,#14084,#14085);
#10960=AXIS2_PLACEMENT_3D('',#17684,#14086,#14087);
#10961=AXIS2_PLACEMENT_3D('',#17685,#14088,#14089);
#10962=AXIS2_PLACEMENT_3D('',#17688,#14090,#14091);
#10963=AXIS2_PLACEMENT_3D('',#17690,#14092,#14093);
#10964=AXIS2_PLACEMENT_3D('',#17691,#14094,#14095);
#10965=AXIS2_PLACEMENT_3D('',#17692,#14096,#14097);
#10966=AXIS2_PLACEMENT_3D('',#17695,#14100,#14101);
#10967=AXIS2_PLACEMENT_3D('',#17698,#14102,#14103);
#10968=AXIS2_PLACEMENT_3D('',#17700,#14104,#14105);
#10969=AXIS2_PLACEMENT_3D('',#17701,#14106,#14107);
#10970=AXIS2_PLACEMENT_3D('',#17702,#14108,#14109);
#10971=AXIS2_PLACEMENT_3D('',#17704,#14110,#14111);
#10972=AXIS2_PLACEMENT_3D('',#17706,#14112,#14113);
#10973=AXIS2_PLACEMENT_3D('',#17707,#14114,#14115);
#10974=AXIS2_PLACEMENT_3D('',#17708,#14116,#14117);
#10975=AXIS2_PLACEMENT_3D('',#17711,#14118,#14119);
#10976=AXIS2_PLACEMENT_3D('',#17713,#14120,#14121);
#10977=AXIS2_PLACEMENT_3D('',#17714,#14122,#14123);
#10978=AXIS2_PLACEMENT_3D('',#17715,#14124,#14125);
#10979=AXIS2_PLACEMENT_3D('',#17718,#14126,#14127);
#10980=AXIS2_PLACEMENT_3D('',#17720,#14128,#14129);
#10981=AXIS2_PLACEMENT_3D('',#17721,#14130,#14131);
#10982=AXIS2_PLACEMENT_3D('',#17722,#14132,#14133);
#10983=AXIS2_PLACEMENT_3D('',#17725,#14136,#14137);
#10984=AXIS2_PLACEMENT_3D('',#17728,#14138,#14139);
#10985=AXIS2_PLACEMENT_3D('',#17730,#14140,#14141);
#10986=AXIS2_PLACEMENT_3D('',#17731,#14142,#14143);
#10987=AXIS2_PLACEMENT_3D('',#17732,#14144,#14145);
#10988=AXIS2_PLACEMENT_3D('',#17735,#14148,#14149);
#10989=AXIS2_PLACEMENT_3D('',#17738,#14152,#14153);
#10990=AXIS2_PLACEMENT_3D('',#17741,#14156,#14157);
#10991=AXIS2_PLACEMENT_3D('',#17744,#14160,#14161);
#10992=AXIS2_PLACEMENT_3D('',#17747,#14164,#14165);
#10993=AXIS2_PLACEMENT_3D('',#17750,#14168,#14169);
#10994=AXIS2_PLACEMENT_3D('',#17752,#14171,#14172);
#10995=AXIS2_PLACEMENT_3D('',#17754,#14174,#14175);
#10996=AXIS2_PLACEMENT_3D('',#17757,#14178,#14179);
#10997=AXIS2_PLACEMENT_3D('',#17760,#14182,#14183);
#10998=AXIS2_PLACEMENT_3D('',#17762,#14185,#14186);
#10999=AXIS2_PLACEMENT_3D('',#17764,#14188,#14189);
#11000=AXIS2_PLACEMENT_3D('',#17769,#14192,#14193);
#11001=AXIS2_PLACEMENT_3D('',#17770,#14194,#14195);
#11002=AXIS2_PLACEMENT_3D('',#17773,#14198,#14199);
#11003=AXIS2_PLACEMENT_3D('',#17775,#14201,#14202);
#11004=AXIS2_PLACEMENT_3D('',#17776,#14203,#14204);
#11005=AXIS2_PLACEMENT_3D('',#17777,#14205,#14206);
#11006=AXIS2_PLACEMENT_3D('',#17782,#14208,#14209);
#11007=AXIS2_PLACEMENT_3D('',#17785,#14211,#14212);
#11008=AXIS2_PLACEMENT_3D('',#17786,#14213,#14214);
#11009=AXIS2_PLACEMENT_3D('',#17787,#14215,#14216);
#11010=AXIS2_PLACEMENT_3D('',#17788,#14217,#14218);
#11011=AXIS2_PLACEMENT_3D('',#17789,#14219,#14220);
#11012=AXIS2_PLACEMENT_3D('',#17790,#14221,#14222);
#11013=AXIS2_PLACEMENT_3D('',#17791,#14223,#14224);
#11014=AXIS2_PLACEMENT_3D('',#17793,#14225,#14226);
#11015=AXIS2_PLACEMENT_3D('',#17794,#14227,#14228);
#11016=AXIS2_PLACEMENT_3D('',#17795,#14229,#14230);
#11017=AXIS2_PLACEMENT_3D('',#17796,#14231,#14232);
#11018=AXIS2_PLACEMENT_3D('',#17798,#14234,#14235);
#11019=AXIS2_PLACEMENT_3D('',#17799,#14236,#14237);
#11020=AXIS2_PLACEMENT_3D('',#17801,#14239,#14240);
#11021=AXIS2_PLACEMENT_3D('',#17802,#14241,#14242);
#14000=DIRECTION('axis',(0.,0.,1.));
#14001=DIRECTION('refdir',(1.,0.,0.));
#14002=DIRECTION('center_axis',(-1.,0.,0.));
#14003=DIRECTION('ref_axis',(0.,-0.707106781186519,-0.707106781186576));
#14004=DIRECTION('center_axis',(-1.,0.,0.));
#14005=DIRECTION('ref_axis',(0.,0.,-1.));
#14006=DIRECTION('',(-1.,0.,0.));
#14007=DIRECTION('center_axis',(1.,0.,0.));
#14008=DIRECTION('ref_axis',(0.,-1.,0.));
#14009=DIRECTION('',(1.,0.,0.));
#14010=DIRECTION('center_axis',(0.,0.,1.));
#14011=DIRECTION('ref_axis',(-1.,0.,0.));
#14012=DIRECTION('center_axis',(-1.,0.,0.));
#14013=DIRECTION('ref_axis',(0.,1.,0.));
#14014=DIRECTION('center_axis',(0.,0.,-1.));
#14015=DIRECTION('ref_axis',(-1.,0.,0.));
#14016=DIRECTION('center_axis',(0.,0.,1.));
#14017=DIRECTION('ref_axis',(-1.,0.,0.));
#14018=DIRECTION('center_axis',(1.,0.,0.));
#14019=DIRECTION('ref_axis',(0.,0.707106781186561,-0.707106781186534));
#14020=DIRECTION('center_axis',(-1.,0.,0.));
#14021=DIRECTION('ref_axis',(0.,1.,0.));
#14022=DIRECTION('',(-1.,0.,0.));
#14023=DIRECTION('',(1.,0.,0.));
#14024=DIRECTION('center_axis',(0.,0.,1.));
#14025=DIRECTION('ref_axis',(1.,0.,0.));
#14026=DIRECTION('center_axis',(0.,0.,-1.));
#14027=DIRECTION('ref_axis',(1.,0.,0.));
#14028=DIRECTION('center_axis',(0.,0.,1.));
#14029=DIRECTION('ref_axis',(1.,0.,0.));
#14030=DIRECTION('center_axis',(0.,0.,-1.));
#14031=DIRECTION('ref_axis',(0.,1.,0.));
#14032=DIRECTION('',(0.,0.,-1.));
#14033=DIRECTION('center_axis',(0.,0.,-1.));
#14034=DIRECTION('ref_axis',(-1.,0.,0.));
#14035=DIRECTION('',(0.,0.,-1.));
#14036=DIRECTION('center_axis',(0.,1.,0.));
#14037=DIRECTION('ref_axis',(1.,0.,0.));
#14038=DIRECTION('',(0.,0.,-1.));
#14039=DIRECTION('',(1.,0.,0.));
#14040=DIRECTION('center_axis',(0.,0.,-1.));
#14041=DIRECTION('ref_axis',(1.,0.,0.));
#14042=DIRECTION('',(-1.,0.,0.));
#14043=DIRECTION('',(0.,1.,0.));
#14044=DIRECTION('',(1.,0.,0.));
#14045=DIRECTION('',(0.,-1.,0.));
#14046=DIRECTION('center_axis',(0.,1.,0.));
#14047=DIRECTION('ref_axis',(0.,0.,-1.));
#14048=DIRECTION('center_axis',(-1.,0.,0.));
#14049=DIRECTION('ref_axis',(0.,0.,-1.));
#14050=DIRECTION('center_axis',(0.,1.,0.));
#14051=DIRECTION('ref_axis',(1.,0.,0.));
#14052=DIRECTION('center_axis',(0.,0.,-1.));
#14053=DIRECTION('ref_axis',(0.,-1.,0.));
#14054=DIRECTION('center_axis',(0.,-1.,0.));
#14055=DIRECTION('ref_axis',(0.70710678118654,0.,0.707106781186555));
#14056=DIRECTION('center_axis',(0.816496580927734,0.408248290463867,0.408248290463843));
#14057=DIRECTION('ref_axis',(0.577350269189598,-0.577350269189645,-0.577350269189634));
#14058=DIRECTION('center_axis',(1.,0.,0.));
#14059=DIRECTION('ref_axis',(0.,0.,-1.));
#14060=DIRECTION('center_axis',(0.,-1.,0.));
#14061=DIRECTION('ref_axis',(1.,0.,0.));
#14062=DIRECTION('center_axis',(9.25185853854317E-16,0.,-1.));
#14063=DIRECTION('ref_axis',(0.,-1.,0.));
#14064=DIRECTION('center_axis',(0.,1.,0.));
#14065=DIRECTION('ref_axis',(0.,0.,-1.));
#14066=DIRECTION('center_axis',(0.,1.,0.));
#14067=DIRECTION('ref_axis',(0.70710678118654,0.,0.707106781186555));
#14068=DIRECTION('center_axis',(0.,0.,-1.));
#14069=DIRECTION('ref_axis',(-1.,0.,0.));
#14070=DIRECTION('center_axis',(5.92118946466763E-14,-1.,0.));
#14071=DIRECTION('ref_axis',(0.,0.,1.));
#14072=DIRECTION('center_axis',(-1.,0.,0.));
#14073=DIRECTION('ref_axis',(0.,1.,0.));
#14074=DIRECTION('center_axis',(0.,0.,-1.));
#14075=DIRECTION('ref_axis',(-0.707106781186547,0.707106781186547,0.));
#14076=DIRECTION('',(0.,0.,1.));
#14077=DIRECTION('',(0.,0.,-1.));
#14078=DIRECTION('center_axis',(-0.707106781186576,0.,0.707106781186519));
#14079=DIRECTION('ref_axis',(0.707106781186519,0.,0.707106781186576));
#14080=DIRECTION('center_axis',(0.827465426020362,-0.538877990790925,-0.157833709270471));
#14081=DIRECTION('ref_axis',(-0.561516668266355,-0.794104487760816,-0.232587819494453));
#14082=DIRECTION('center_axis',(-0.707106781186544,3.663549070262E-14,-0.707106781186551));
#14083=DIRECTION('ref_axis',(-0.707106781186551,0.,0.707106781186544));
#14084=DIRECTION('center_axis',(0.,-1.,0.));
#14085=DIRECTION('ref_axis',(0.,0.,-1.));
#14086=DIRECTION('center_axis',(-1.,0.,-2.96059473233375E-14));
#14087=DIRECTION('ref_axis',(0.,-1.,0.));
#14088=DIRECTION('center_axis',(-0.408248290463871,-0.408248290463824,-0.816496580927742));
#14089=DIRECTION('ref_axis',(0.577350269189681,0.577350269189586,-0.57735026918961));
#14090=DIRECTION('center_axis',(0.,1.,0.));
#14091=DIRECTION('ref_axis',(0.,0.,-1.));
#14092=DIRECTION('center_axis',(1.,0.,5.9211894646675E-14));
#14093=DIRECTION('ref_axis',(0.,1.,0.));
#14094=DIRECTION('center_axis',(0.,9.25185853854317E-16,-1.));
#14095=DIRECTION('ref_axis',(1.,0.,0.));
#14096=DIRECTION('center_axis',(1.,0.,0.));
#14097=DIRECTION('ref_axis',(0.,0.707106781186519,-0.707106781186576));
#14098=DIRECTION('',(1.,0.,0.));
#14099=DIRECTION('',(-1.,0.,0.));
#14100=DIRECTION('center_axis',(0.408248290463859,-0.408248290463835,-0.816496580927742));
#14101=DIRECTION('ref_axis',(0.577350269189665,-0.577350269189618,0.577350269189594));
#14102=DIRECTION('center_axis',(0.,0.,1.));
#14103=DIRECTION('ref_axis',(1.,0.,0.));
#14104=DIRECTION('center_axis',(0.,-1.,0.));
#14105=DIRECTION('ref_axis',(0.,0.,1.));
#14106=DIRECTION('center_axis',(1.,0.,5.9211894646675E-14));
#14107=DIRECTION('ref_axis',(0.,-1.,0.));
#14108=DIRECTION('center_axis',(0.827465426020388,0.538877990790895,-0.157833709270442));
#14109=DIRECTION('ref_axis',(-0.561516668266318,0.794104487760845,-0.232587819494444));
#14110=DIRECTION('center_axis',(0.,1.,0.));
#14111=DIRECTION('ref_axis',(-0.707106781186544,0.,0.707106781186551));
#14112=DIRECTION('center_axis',(-0.70710678118657,0.,-0.707106781186525));
#14113=DIRECTION('ref_axis',(0.,1.,0.));
#14114=DIRECTION('center_axis',(-1.,-2.96059473233364E-14,0.));
#14115=DIRECTION('ref_axis',(0.,0.,-1.));
#14116=DIRECTION('center_axis',(-0.182143211721521,0.879465224064606,0.439732612032315));
#14117=DIRECTION('ref_axis',(-0.336556770590777,-0.475963149477983,0.812519920068737));
#14118=DIRECTION('center_axis',(-1.,0.,0.));
#14119=DIRECTION('ref_axis',(0.,0.,1.));
#14120=DIRECTION('center_axis',(0.,-1.,0.));
#14121=DIRECTION('ref_axis',(-0.707106781186551,0.,0.707106781186544));
#14122=DIRECTION('center_axis',(0.70710678118654,0.,0.707106781186555));
#14123=DIRECTION('ref_axis',(0.,-1.,0.));
#14124=DIRECTION('center_axis',(0.408248290463908,0.408248290463861,-0.816496580927704));
#14125=DIRECTION('ref_axis',(0.577350269189642,0.577350269189594,0.577350269189642));
#14126=DIRECTION('center_axis',(0.,1.,5.9211894646675E-14));
#14127=DIRECTION('ref_axis',(1.,0.,0.));
#14128=DIRECTION('center_axis',(0.,0.,1.));
#14129=DIRECTION('ref_axis',(0.,1.,0.));
#14130=DIRECTION('center_axis',(1.,0.,0.));
#14131=DIRECTION('ref_axis',(0.,0.,1.));
#14132=DIRECTION('center_axis',(0.,0.,1.));
#14133=DIRECTION('ref_axis',(0.707106781186589,0.707106781186506,0.));
#14134=DIRECTION('',(0.,0.,-1.));
#14135=DIRECTION('',(0.,0.,1.));
#14136=DIRECTION('center_axis',(0.182143211721517,0.879465224064606,-0.439732612032315));
#14137=DIRECTION('ref_axis',(-0.336556770590767,0.475963149477992,0.812519920068736));
#14138=DIRECTION('center_axis',(0.,1.,0.));
#14139=DIRECTION('ref_axis',(0.,0.,1.));
#14140=DIRECTION('center_axis',(-1.,0.,0.));
#14141=DIRECTION('ref_axis',(0.,1.,0.));
#14142=DIRECTION('center_axis',(0.70710678118654,0.,0.707106781186555));
#14143=DIRECTION('ref_axis',(-0.707106781186555,0.,0.70710678118654));
#14144=DIRECTION('center_axis',(1.,0.,0.));
#14145=DIRECTION('ref_axis',(0.,0.707106781186558,0.707106781186537));
#14146=DIRECTION('',(-1.,0.,0.));
#14147=DIRECTION('',(1.,0.,0.));
#14148=DIRECTION('center_axis',(0.707106781186547,0.,0.707106781186548));
#14149=DIRECTION('ref_axis',(-0.499999999999997,0.707106781186559,0.499999999999986));
#14150=DIRECTION('',(-0.707106781186547,0.,-0.707106781186548));
#14151=DIRECTION('',(0.707106781186547,0.,0.707106781186548));
#14152=DIRECTION('center_axis',(0.,-1.,0.));
#14153=DIRECTION('ref_axis',(-0.382683432365094,0.,0.923879532511285));
#14154=DIRECTION('',(0.,1.,0.));
#14155=DIRECTION('',(0.,-1.,0.));
#14156=DIRECTION('center_axis',(0.,-1.,0.));
#14157=DIRECTION('ref_axis',(0.707106781186558,0.,0.707106781186537));
#14158=DIRECTION('',(0.,1.,0.));
#14159=DIRECTION('',(0.,-1.,0.));
#14160=DIRECTION('center_axis',(-0.707106781186547,0.,-0.707106781186548));
#14161=DIRECTION('ref_axis',(-0.499999999999997,-0.707106781186559,0.499999999999986));
#14162=DIRECTION('',(0.707106781186547,0.,0.707106781186548));
#14163=DIRECTION('',(-0.707106781186547,0.,-0.707106781186548));
#14164=DIRECTION('center_axis',(-1.,0.,0.));
#14165=DIRECTION('ref_axis',(0.,-0.707106781186558,0.707106781186537));
#14166=DIRECTION('',(1.,0.,0.));
#14167=DIRECTION('',(-1.,0.,0.));
#14168=DIRECTION('center_axis',(-1.,0.,0.));
#14169=DIRECTION('ref_axis',(0.,0.707106781186561,-0.707106781186534));
#14170=DIRECTION('',(1.,0.,0.));
#14171=DIRECTION('center_axis',(0.,-1.,0.));
#14172=DIRECTION('ref_axis',(-0.923879532511297,0.,-0.382683432365066));
#14173=DIRECTION('',(0.,1.,0.));
#14174=DIRECTION('center_axis',(0.,0.,1.));
#14175=DIRECTION('ref_axis',(0.707106781186506,-0.707106781186589,0.));
#14176=DIRECTION('',(0.,0.,-1.));
#14177=DIRECTION('',(0.,0.,1.));
#14178=DIRECTION('center_axis',(0.,-1.,0.));
#14179=DIRECTION('ref_axis',(0.707106781186519,0.,-0.707106781186576));
#14180=DIRECTION('',(0.,1.,0.));
#14181=DIRECTION('',(0.,-1.,0.));
#14182=DIRECTION('center_axis',(1.,0.,0.));
#14183=DIRECTION('ref_axis',(0.,-0.707106781186561,-0.707106781186534));
#14184=DIRECTION('',(-1.,0.,0.));
#14185=DIRECTION('center_axis',(0.,-1.,0.));
#14186=DIRECTION('ref_axis',(0.707106781186519,0.,0.707106781186576));
#14187=DIRECTION('',(0.,-1.,0.));
#14188=DIRECTION('center_axis',(1.,0.,0.));
#14189=DIRECTION('ref_axis',(0.,-0.707106781186561,-0.707106781186534));
#14190=DIRECTION('',(1.,0.,0.));
#14191=DIRECTION('',(-1.,0.,0.));
#14192=DIRECTION('center_axis',(0.707106781186555,0.,-0.70710678118654));
#14193=DIRECTION('ref_axis',(-0.70710678118654,0.,-0.707106781186555));
#14194=DIRECTION('center_axis',(0.,0.,-1.));
#14195=DIRECTION('ref_axis',(-0.707106781186506,-0.707106781186589,0.));
#14196=DIRECTION('',(0.,0.,1.));
#14197=DIRECTION('',(0.,0.,-1.));
#14198=DIRECTION('center_axis',(-1.,0.,0.));
#14199=DIRECTION('ref_axis',(0.,0.,-1.));
#14200=DIRECTION('',(0.,-1.,0.));
#14201=DIRECTION('center_axis',(0.,-1.,0.));
#14202=DIRECTION('ref_axis',(-1.,0.,0.));
#14203=DIRECTION('center_axis',(1.,0.,0.));
#14204=DIRECTION('ref_axis',(0.,0.,1.));
#14205=DIRECTION('center_axis',(0.,0.,1.));
#14206=DIRECTION('ref_axis',(-1.,0.,0.));
#14207=DIRECTION('',(-1.,0.,0.));
#14208=DIRECTION('center_axis',(0.,0.,1.));
#14209=DIRECTION('ref_axis',(1.,0.,0.));
#14210=DIRECTION('',(1.,0.,0.));
#14211=DIRECTION('center_axis',(0.,0.,1.));
#14212=DIRECTION('ref_axis',(-1.,0.,0.));
#14213=DIRECTION('center_axis',(-0.707106781186548,0.,0.707106781186547));
#14214=DIRECTION('ref_axis',(-0.707106781186547,0.,-0.707106781186548));
#14215=DIRECTION('center_axis',(0.,-1.,0.));
#14216=DIRECTION('ref_axis',(0.,0.,1.));
#14217=DIRECTION('center_axis',(1.,0.,0.));
#14218=DIRECTION('ref_axis',(0.,-0.707106781186516,0.707106781186579));
#14219=DIRECTION('center_axis',(1.,0.,0.));
#14220=DIRECTION('ref_axis',(0.,0.,1.));
#14221=DIRECTION('center_axis',(-1.,0.,0.));
#14222=DIRECTION('ref_axis',(0.,-1.,0.));
#14223=DIRECTION('center_axis',(0.,0.,-1.));
#14224=DIRECTION('ref_axis',(1.,0.,0.));
#14225=DIRECTION('center_axis',(1.,0.,0.));
#14226=DIRECTION('ref_axis',(0.,1.,0.));
#14227=DIRECTION('center_axis',(0.,0.,-1.));
#14228=DIRECTION('ref_axis',(1.,0.,0.));
#14229=DIRECTION('center_axis',(-1.,0.,0.));
#14230=DIRECTION('ref_axis',(0.,0.707106781186558,0.707106781186537));
#14231=DIRECTION('center_axis',(1.,0.,0.));
#14232=DIRECTION('ref_axis',(0.,1.,0.));
#14233=DIRECTION('',(-1.,0.,0.));
#14234=DIRECTION('center_axis',(0.,0.,-1.));
#14235=DIRECTION('ref_axis',(-1.,0.,0.));
#14236=DIRECTION('center_axis',(0.,0.,-1.));
#14237=DIRECTION('ref_axis',(0.,-1.,0.));
#14238=DIRECTION('',(0.,0.,-1.));
#14239=DIRECTION('center_axis',(0.,-1.,0.));
#14240=DIRECTION('ref_axis',(-1.,0.,0.));
#14241=DIRECTION('center_axis',(0.,0.,-1.));
#14242=DIRECTION('ref_axis',(1.,0.,0.));
#17606=CARTESIAN_POINT('',(0.,0.,0.));
#17607=CARTESIAN_POINT('Origin',(69.9040264336917,64.8,3.08953555269655));
#17608=CARTESIAN_POINT('',(104.475451921837,64.8,2.78953555269655));
#17609=CARTESIAN_POINT('',(104.475451921837,64.5,3.08953555269655));
#17610=CARTESIAN_POINT('Origin',(104.475451921837,64.8,3.08953555269655));
#17611=CARTESIAN_POINT('',(77.8080528673835,64.5,3.08953555269655));
#17612=CARTESIAN_POINT('',(69.9040264336917,64.5,3.08953555269655));
#17613=CARTESIAN_POINT('',(77.8080528673835,64.8,2.78953555269655));
#17614=CARTESIAN_POINT('Origin',(77.8080528673835,64.8,3.08953555269655));
#17615=CARTESIAN_POINT('',(69.9040264336917,64.8,2.78953555269655));
#17616=CARTESIAN_POINT('Origin',(77.8080528673835,60.,3.08953555269655));
#17617=CARTESIAN_POINT('',(77.8080528673835,55.5,3.08953555269655));
#17618=CARTESIAN_POINT('',(77.8080528673835,55.2,2.78953555269655));
#17619=CARTESIAN_POINT('Origin',(77.8080528673835,55.2,3.08953555269655));
#17620=CARTESIAN_POINT('Origin',(77.8080528673835,60.,2.78953555269655));
#17621=CARTESIAN_POINT('Origin',(77.8080528673835,60.,3.08953555269655));
#17622=CARTESIAN_POINT('Origin',(83.2377259609183,55.2,3.08953555269655));
#17623=CARTESIAN_POINT('',(104.475451921837,55.5,3.08953555269655));
#17624=CARTESIAN_POINT('',(104.475451921837,55.2,2.78953555269655));
#17625=CARTESIAN_POINT('Origin',(104.475451921837,55.2,3.08953555269655));
#17626=CARTESIAN_POINT('',(83.2377259609183,55.2,2.78953555269655));
#17627=CARTESIAN_POINT('',(83.2377259609183,55.5,3.08953555269655));
#17628=CARTESIAN_POINT('Origin',(104.475451921837,60.,3.08953555269655));
#17629=CARTESIAN_POINT('Origin',(104.475451921837,60.,2.78953555269655));
#17630=CARTESIAN_POINT('Origin',(104.475451921837,60.,3.08953555269655));
#17631=CARTESIAN_POINT('Origin',(77.8080528673835,60.,10.7895355526966));
#17632=CARTESIAN_POINT('',(77.8080528673835,64.5,10.4895355526966));
#17633=CARTESIAN_POINT('',(77.8080528673835,64.5,10.7895355526966));
#17634=CARTESIAN_POINT('',(77.8080528673835,55.5,10.4895355526966));
#17635=CARTESIAN_POINT('Origin',(77.8080528673835,60.,10.4895355526966));
#17636=CARTESIAN_POINT('',(77.8080528673835,55.5,10.7895355526966));
#17637=CARTESIAN_POINT('Origin',(77.8080528673835,64.5,10.7895355526966));
#17638=CARTESIAN_POINT('',(104.475451921837,64.5,10.4895355526966));
#17639=CARTESIAN_POINT('',(104.475451921837,64.5,10.7895355526966));
#17640=CARTESIAN_POINT('',(94.9040264336917,64.5,10.4895355526966));
#17641=CARTESIAN_POINT('Origin',(62.,70.,2.78953555269655));
#17642=CARTESIAN_POINT('',(109.7,69.7,2.78953555269655));
#17643=CARTESIAN_POINT('',(62.7242640687119,69.7,2.78953555269655));
#17644=CARTESIAN_POINT('',(74.5,69.7,2.78953555269655));
#17645=CARTESIAN_POINT('',(109.7,50.3,2.78953555269655));
#17646=CARTESIAN_POINT('',(109.7,70.,2.78953555269655));
#17647=CARTESIAN_POINT('',(62.7242640687119,50.3,2.78953555269655));
#17648=CARTESIAN_POINT('',(74.5,50.3,2.78953555269655));
#17649=CARTESIAN_POINT('',(62.7242640687119,70.,2.78953555269655));
#17650=CARTESIAN_POINT('Origin',(109.7,50.3,2.48953555269655));
#17651=CARTESIAN_POINT('',(109.7,50.,3.08953555269655));
#17652=CARTESIAN_POINT('Origin',(109.7,50.3,3.08953555269655));
#17653=CARTESIAN_POINT('',(110.,50.3,2.48953555269655));
#17654=CARTESIAN_POINT('Origin',(109.7,50.3,2.48953555269655));
#17655=CARTESIAN_POINT('',(110.3,50.,2.48953555269655));
#17656=CARTESIAN_POINT('Origin',(110.3,50.3,2.48953555269655));
#17657=CARTESIAN_POINT('Origin',(109.7,50.,2.48953555269655));
#17658=CARTESIAN_POINT('Origin',(111.7,50.3,0.3));
#17659=CARTESIAN_POINT('',(111.7,50.3,0.));
#17660=CARTESIAN_POINT('',(111.7,50.,0.3));
#17661=CARTESIAN_POINT('Origin',(111.7,50.3,0.3));
#17662=CARTESIAN_POINT('',(112.,50.3,0.3));
#17663=CARTESIAN_POINT('Origin',(111.7,50.3,0.3));
#17664=CARTESIAN_POINT('Origin',(111.7,50.3,0.3));
#17665=CARTESIAN_POINT('Origin',(109.7,69.7,2.48953555269655));
#17666=CARTESIAN_POINT('',(109.7,70.,3.08953555269655));
#17667=CARTESIAN_POINT('',(110.3,70.,2.48953555269655));
#17668=CARTESIAN_POINT('Origin',(109.7,70.,2.48953555269655));
#17669=CARTESIAN_POINT('',(110.,69.7,2.48953555269655));
#17670=CARTESIAN_POINT('Origin',(110.3,69.7,2.48953555269655));
#17671=CARTESIAN_POINT('Origin',(109.7,69.7,2.48953555269655));
#17672=CARTESIAN_POINT('Origin',(109.7,69.7,3.08953555269655));
#17673=CARTESIAN_POINT('Origin',(110.3,69.7,4.09215166452241));
#17674=CARTESIAN_POINT('',(110.,69.7,0.));
#17675=CARTESIAN_POINT('',(110.,69.7,4.09215166452241));
#17676=CARTESIAN_POINT('',(110.3,70.,0.3));
#17677=CARTESIAN_POINT('',(110.3,70.,4.09215166452241));
#17678=CARTESIAN_POINT('Origin',(110.3,69.7,0.3));
#17679=CARTESIAN_POINT('Origin',(62.7242640687119,50.3,3.08953555269655));
#17680=CARTESIAN_POINT('',(62.512132034356,50.3,3.30166758705252));
#17681=CARTESIAN_POINT('',(62.7242640687119,50.,3.08953555269655));
#17682=CARTESIAN_POINT('Origin',(62.7242640687119,50.3,3.08953555269656));
#17683=CARTESIAN_POINT('Origin',(62.7242640687119,50.3,3.08953555269655));
#17684=CARTESIAN_POINT('Origin',(62.7242640687119,50.3,3.08953555269655));
#17685=CARTESIAN_POINT('Origin',(111.7,69.7,0.3));
#17686=CARTESIAN_POINT('',(111.7,69.7,0.));
#17687=CARTESIAN_POINT('',(112.,69.7,0.3));
#17688=CARTESIAN_POINT('Origin',(111.7,69.7,0.3));
#17689=CARTESIAN_POINT('',(111.7,70.,0.3));
#17690=CARTESIAN_POINT('Origin',(111.7,69.7,0.3));
#17691=CARTESIAN_POINT('Origin',(111.7,69.7,0.3));
#17692=CARTESIAN_POINT('Origin',(98.5,69.7,0.3));
#17693=CARTESIAN_POINT('',(98.5,70.,0.3));
#17694=CARTESIAN_POINT('',(98.5,69.7,0.));
#17695=CARTESIAN_POINT('Origin',(111.7,50.3,10.4895355526966));
#17696=CARTESIAN_POINT('',(112.,50.3,10.4895355526966));
#17697=CARTESIAN_POINT('',(111.7,50.,10.4895355526966));
#17698=CARTESIAN_POINT('Origin',(111.7,50.3,10.4895355526966));
#17699=CARTESIAN_POINT('',(111.7,50.3,10.7895355526966));
#17700=CARTESIAN_POINT('Origin',(111.7,50.3,10.4895355526966));
#17701=CARTESIAN_POINT('Origin',(111.7,50.3,10.4895355526966));
#17702=CARTESIAN_POINT('Origin',(62.7242640687119,69.7,3.08953555269655));
#17703=CARTESIAN_POINT('',(62.512132034356,69.7,3.30166758705252));
#17704=CARTESIAN_POINT('Origin',(62.7242640687119,69.7,3.08953555269655));
#17705=CARTESIAN_POINT('',(62.7242640687119,70.,3.08953555269655));
#17706=CARTESIAN_POINT('Origin',(62.7242640687119,69.7,3.08953555269655));
#17707=CARTESIAN_POINT('Origin',(62.7242640687119,69.7,3.08953555269655));
#17708=CARTESIAN_POINT('Origin',(70.1242640687119,50.3,10.4895355526966));
#17709=CARTESIAN_POINT('',(70.1242640687119,50.3,10.7895355526966));
#17710=CARTESIAN_POINT('',(70.1242640687119,50.,10.4895355526966));
#17711=CARTESIAN_POINT('Origin',(70.1242640687119,50.3,10.4895355526966));
#17712=CARTESIAN_POINT('',(69.9121320343559,50.3,10.7016675870525));
#17713=CARTESIAN_POINT('Origin',(70.1242640687119,50.3,10.4895355526966));
#17714=CARTESIAN_POINT('Origin',(70.1242640687119,50.3,10.4895355526966));
#17715=CARTESIAN_POINT('Origin',(111.7,69.7,10.4895355526966));
#17716=CARTESIAN_POINT('',(112.,69.7,10.4895355526966));
#17717=CARTESIAN_POINT('',(111.7,69.7,10.7895355526966));
#17718=CARTESIAN_POINT('Origin',(111.7,69.7,10.4895355526966));
#17719=CARTESIAN_POINT('',(111.7,70.,10.4895355526966));
#17720=CARTESIAN_POINT('Origin',(111.7,69.7,10.4895355526966));
#17721=CARTESIAN_POINT('Origin',(111.7,69.7,10.4895355526966));
#17722=CARTESIAN_POINT('Origin',(111.7,69.7,2.69738388817414));
#17723=CARTESIAN_POINT('',(112.,69.7,2.69738388817414));
#17724=CARTESIAN_POINT('',(111.7,70.,2.69738388817414));
#17725=CARTESIAN_POINT('Origin',(70.1242640687119,69.7,10.4895355526966));
#17726=CARTESIAN_POINT('',(70.1242640687119,69.7,10.7895355526966));
#17727=CARTESIAN_POINT('',(69.9121320343559,69.7,10.7016675870525));
#17728=CARTESIAN_POINT('Origin',(70.1242640687119,69.7,10.4895355526966));
#17729=CARTESIAN_POINT('',(70.1242640687119,70.,10.4895355526966));
#17730=CARTESIAN_POINT('Origin',(70.1242640687119,69.7,10.4895355526966));
#17731=CARTESIAN_POINT('Origin',(70.1242640687119,69.7,10.4895355526966));
#17732=CARTESIAN_POINT('Origin',(99.5,69.7,10.4895355526966));
#17733=CARTESIAN_POINT('',(99.5,70.,10.4895355526966));
#17734=CARTESIAN_POINT('',(99.5,69.7,10.7895355526966));
#17735=CARTESIAN_POINT('Origin',(73.1134400902689,69.7,13.4787115742535));
#17736=CARTESIAN_POINT('',(73.1134400902689,70.,13.4787115742535));
#17737=CARTESIAN_POINT('',(72.9013080559129,69.7,13.6908436086095));
#17738=CARTESIAN_POINT('Origin',(70.1242640687119,70.,10.4895355526966));
#17739=CARTESIAN_POINT('',(70.1242640687119,70.,10.7895355526966));
#17740=CARTESIAN_POINT('',(69.9121320343559,70.,10.7016675870525));
#17741=CARTESIAN_POINT('Origin',(111.7,70.,10.4895355526966));
#17742=CARTESIAN_POINT('',(112.,70.,10.4895355526966));
#17743=CARTESIAN_POINT('',(111.7,70.,10.7895355526966));
#17744=CARTESIAN_POINT('Origin',(73.1134400902689,50.3,13.4787115742535));
#17745=CARTESIAN_POINT('',(73.1134400902689,50.,13.4787115742535));
#17746=CARTESIAN_POINT('',(72.9013080559129,50.3,13.6908436086095));
#17747=CARTESIAN_POINT('Origin',(99.5,50.3,10.4895355526966));
#17748=CARTESIAN_POINT('',(99.5,50.,10.4895355526966));
#17749=CARTESIAN_POINT('',(99.5,50.3,10.7895355526966));
#17750=CARTESIAN_POINT('Origin',(74.5,69.7,3.08953555269655));
#17751=CARTESIAN_POINT('',(74.5,70.,3.08953555269655));
#17752=CARTESIAN_POINT('Origin',(62.7242640687119,70.,3.08953555269655));
#17753=CARTESIAN_POINT('',(62.512132034356,70.,3.30166758705252));
#17754=CARTESIAN_POINT('Origin',(111.7,50.3,2.69738388817414));
#17755=CARTESIAN_POINT('',(111.7,50.,2.69738388817414));
#17756=CARTESIAN_POINT('',(112.,50.3,2.69738388817414));
#17757=CARTESIAN_POINT('Origin',(111.7,70.,0.3));
#17758=CARTESIAN_POINT('',(111.7,70.,0.));
#17759=CARTESIAN_POINT('',(112.,70.,0.3));
#17760=CARTESIAN_POINT('Origin',(74.5,50.3,3.08953555269655));
#17761=CARTESIAN_POINT('',(74.5,50.,3.08953555269655));
#17762=CARTESIAN_POINT('Origin',(109.7,70.,2.48953555269655));
#17763=CARTESIAN_POINT('',(110.,70.,2.48953555269655));
#17764=CARTESIAN_POINT('Origin',(98.5,50.3,0.3));
#17765=CARTESIAN_POINT('',(110.,50.3,0.));
#17766=CARTESIAN_POINT('',(98.5,50.3,0.));
#17767=CARTESIAN_POINT('',(110.3,50.,0.3));
#17768=CARTESIAN_POINT('',(98.5,50.,0.3));
#17769=CARTESIAN_POINT('Origin',(110.3,50.3,0.3));
#17770=CARTESIAN_POINT('Origin',(110.3,50.3,4.09215166452241));
#17771=CARTESIAN_POINT('',(110.3,50.,4.09215166452241));
#17772=CARTESIAN_POINT('',(110.,50.3,4.09215166452241));
#17773=CARTESIAN_POINT('Origin',(110.,70.,2.78953555269655));
#17774=CARTESIAN_POINT('',(110.,70.,0.));
#17775=CARTESIAN_POINT('Origin',(87.,70.,5.39476777634828));
#17776=CARTESIAN_POINT('Origin',(112.,70.,0.));
#17777=CARTESIAN_POINT('Origin',(112.,70.,10.7895355526966));
#17778=CARTESIAN_POINT('',(104.475451921837,64.8,10.7895355526966));
#17779=CARTESIAN_POINT('',(77.8080528673835,64.8,10.7895355526966));
#17780=CARTESIAN_POINT('',(94.9040264336917,64.8,10.7895355526966));
#17781=CARTESIAN_POINT('',(104.475451921837,55.2,10.7895355526966));
#17782=CARTESIAN_POINT('Origin',(104.475451921837,60.,10.7895355526966));
#17783=CARTESIAN_POINT('',(77.8080528673835,55.2,10.7895355526966));
#17784=CARTESIAN_POINT('',(108.237725960918,55.2,10.7895355526966));
#17785=CARTESIAN_POINT('Origin',(77.8080528673835,60.,10.7895355526966));
#17786=CARTESIAN_POINT('Origin',(70.,70.,10.7895355526965));
#17787=CARTESIAN_POINT('Origin',(87.,50.,5.39476777634828));
#17788=CARTESIAN_POINT('Origin',(94.9040264336917,64.8,10.4895355526966));
#17789=CARTESIAN_POINT('Origin',(77.8080528673835,64.8,10.4895355526966));
#17790=CARTESIAN_POINT('Origin',(104.475451921837,64.8,10.4895355526966));
#17791=CARTESIAN_POINT('Origin',(104.475451921837,60.,10.4895355526966));
#17792=CARTESIAN_POINT('',(104.475451921837,55.5,10.4895355526966));
#17793=CARTESIAN_POINT('Origin',(104.475451921837,55.2,10.4895355526966));
#17794=CARTESIAN_POINT('Origin',(104.475451921837,60.,10.4895355526966));
#17795=CARTESIAN_POINT('Origin',(108.237725960918,55.2,10.4895355526966));
#17796=CARTESIAN_POINT('Origin',(77.8080528673835,55.2,10.4895355526966));
#17797=CARTESIAN_POINT('',(108.237725960918,55.5,10.4895355526966));
#17798=CARTESIAN_POINT('Origin',(77.8080528673835,60.,10.4895355526966));
#17799=CARTESIAN_POINT('Origin',(104.475451921837,60.,10.7895355526966));
#17800=CARTESIAN_POINT('',(104.475451921837,55.5,10.7895355526966));
#17801=CARTESIAN_POINT('Origin',(104.475451921837,55.5,10.7895355526966));
#17802=CARTESIAN_POINT('Origin',(110.,70.,0.));
#17823=UNCERTAINTY_MEASURE_WITH_UNIT(LENGTH_MEASURE(0.01),#17837,
'DISTANCE_ACCURACY_VALUE',
'Maximum model space distance between geometric entities at asserted c
onnectivities');
#17824=UNCERTAINTY_MEASURE_WITH_UNIT(LENGTH_MEASURE(0.01),#17837,
'DISTANCE_ACCURACY_VALUE',
'Maximum model space distance between geometric entities at asserted c
onnectivities');
#17835=(
GEOMETRIC_REPRESENTATION_CONTEXT(3)
GLOBAL_UNCERTAINTY_ASSIGNED_CONTEXT((#17823))
GLOBAL_UNIT_ASSIGNED_CONTEXT((#17837,#17839,#17840))
REPRESENTATION_CONTEXT('','3D')
);
#17836=(
GEOMETRIC_REPRESENTATION_CONTEXT(3)
GLOBAL_UNCERTAINTY_ASSIGNED_CONTEXT((#17824))
GLOBAL_UNIT_ASSIGNED_CONTEXT((#17837,#17839,#17840))
REPRESENTATION_CONTEXT('','3D')
);
#17837=(
LENGTH_UNIT()
NAMED_UNIT(*)
SI_UNIT(.MILLI.,.METRE.)
);
#17839=(
NAMED_UNIT(*)
PLANE_ANGLE_UNIT()
SI_UNIT($,.RADIAN.)
);
#17840=(
NAMED_UNIT(*)
SI_UNIT($,.STERADIAN.)
SOLID_ANGLE_UNIT()
);
#17851=SHAPE_DEFINITION_REPRESENTATION(#17862,#17883);
#17862=PRODUCT_DEFINITION_SHAPE('',$,#17895);
#17883=SHAPE_REPRESENTATION('',(#10924),#17835);
#17884=PRODUCT_DEFINITION_CONTEXT('part definition',#17919,'design');
#17895=PRODUCT_DEFINITION('Clamp_04','Clamp_04',#17906,#17884);
#17906=PRODUCT_DEFINITION_FORMATION('',$,#17931);
#17919=APPLICATION_CONTEXT(
'Core Data for Automotive Mechanical Design Process');
#17920=PRODUCT_CONTEXT('part definition',#17919,'mechanical');
#17931=PRODUCT('Clamp_04','Clamp_04',$,(#17920));
#17981=COLOUR_RGB('Off White',0.89,0.88,0.83);
#17982=FILL_AREA_STYLE_COLOUR('',#17981);
#17983=FILL_AREA_STYLE('',(#17982));
#17984=SURFACE_STYLE_FILL_AREA(#17983);
#17985=SURFACE_SIDE_STYLE('',(#17984));
#17986=SURFACE_STYLE_USAGE(.BOTH.,#17985);
#17987=PRESENTATION_STYLE_ASSIGNMENT((#17986));
ENDSEC;
END-ISO-10303-21;
